ISO-10303-21;
HEADER;
/* Generated by software containing ST-Developer
 * from STEP Tools, Inc. (www.steptools.com) 
 */

FILE_DESCRIPTION(
/* description */ ('Four-bar parallelogram arm'),
/* implementation_level */ '2;1');

FILE_NAME(
/* name */ '200 mm arm (1).step',
/* time_stamp */ '2026-10-28T03:24:55-07:00',
/* author */ (''),
/* organization */ (''),
/* preprocessor_version */ 'ST-DEVELOPER v20.2',
/* originating_system */ 'Autodesk Translation Framework v15.17.0.0',
/* authorisation */ '');

FILE_SCHEMA (('AUTOMOTIVE_DESIGN { 1 0 10303 214 3 1 1 }'));
ENDSEC;

DATA;
#10=MECHANICAL_DESIGN_GEOMETRIC_PRESENTATION_REPRESENTATION('',(#647),#14512);
#547=SHAPE_REPRESENTATION_RELATIONSHIP('SRR','None',#14770,#597);
#597=ADVANCED_BREP_SHAPE_REPRESENTATION('',(#704),#14485);
#647=STYLED_ITEM('',(#15101),#704);
#704=MANIFOLD_SOLID_BREP('Body1',#7352);
#873=FACE_BOUND('',#1975,.T.);
#874=FACE_BOUND('',#1976,.T.);
#875=FACE_BOUND('',#1977,.T.);
#876=FACE_BOUND('',#1978,.T.);
#877=FACE_BOUND('',#1979,.T.);
#878=FACE_BOUND('',#1980,.T.);
#879=FACE_BOUND('',#1981,.T.);
#880=FACE_BOUND('',#1982,.T.);
#881=FACE_BOUND('',#1983,.T.);
#882=FACE_BOUND('',#1984,.T.);
#883=FACE_BOUND('',#1988,.T.);
#884=FACE_BOUND('',#1989,.T.);
#885=FACE_BOUND('',#1990,.T.);
#886=FACE_BOUND('',#1991,.T.);
#887=FACE_BOUND('',#1992,.T.);
#888=FACE_BOUND('',#1993,.T.);
#889=FACE_BOUND('',#1994,.T.);
#890=FACE_BOUND('',#1995,.T.);
#891=FACE_BOUND('',#1996,.T.);
#892=FACE_BOUND('',#1997,.T.);
#1111=PLANE('',#8397);
#1112=PLANE('',#8398);
#1113=PLANE('',#8400);
#1114=PLANE('',#8403);
#1404=FACE_OUTER_BOUND('',#1962,.T.);
#1405=FACE_OUTER_BOUND('',#1963,.T.);
#1406=FACE_OUTER_BOUND('',#1964,.T.);
#1407=FACE_OUTER_BOUND('',#1965,.T.);
#1408=FACE_OUTER_BOUND('',#1966,.T.);
#1409=FACE_OUTER_BOUND('',#1967,.T.);
#1410=FACE_OUTER_BOUND('',#1968,.T.);
#1411=FACE_OUTER_BOUND('',#1969,.T.);
#1412=FACE_OUTER_BOUND('',#1970,.T.);
#1413=FACE_OUTER_BOUND('',#1971,.T.);
#1414=FACE_OUTER_BOUND('',#1972,.T.);
#1415=FACE_OUTER_BOUND('',#1973,.T.);
#1416=FACE_OUTER_BOUND('',#1974,.T.);
#1417=FACE_OUTER_BOUND('',#1985,.T.);
#1418=FACE_OUTER_BOUND('',#1986,.T.);
#1419=FACE_OUTER_BOUND('',#1987,.T.);
#1962=EDGE_LOOP('',(#5832,#5833,#5834,#5835));
#1963=EDGE_LOOP('',(#5836,#5837,#5838,#5839));
#1964=EDGE_LOOP('',(#5840,#5841,#5842,#5843));
#1965=EDGE_LOOP('',(#5844,#5845,#5846,#5847));
#1966=EDGE_LOOP('',(#5848,#5849,#5850,#5851));
#1967=EDGE_LOOP('',(#5852,#5853,#5854,#5855));
#1968=EDGE_LOOP('',(#5856,#5857,#5858,#5859));
#1969=EDGE_LOOP('',(#5860,#5861,#5862,#5863));
#1970=EDGE_LOOP('',(#5864,#5865,#5866,#5867));
#1971=EDGE_LOOP('',(#5868,#5869,#5870,#5871));
#1972=EDGE_LOOP('',(#5872,#5873,#5874,#5875));
#1973=EDGE_LOOP('',(#5876,#5877,#5878,#5879));
#1974=EDGE_LOOP('',(#5880,#5881,#5882,#5883));
#1975=EDGE_LOOP('',(#5884));
#1976=EDGE_LOOP('',(#5885));
#1977=EDGE_LOOP('',(#5886));
#1978=EDGE_LOOP('',(#5887));
#1979=EDGE_LOOP('',(#5888));
#1980=EDGE_LOOP('',(#5889));
#1981=EDGE_LOOP('',(#5890));
#1982=EDGE_LOOP('',(#5891));
#1983=EDGE_LOOP('',(#5892));
#1984=EDGE_LOOP('',(#5893));
#1985=EDGE_LOOP('',(#5894,#5895,#5896,#5897));
#1986=EDGE_LOOP('',(#5898,#5899,#5900,#5901));
#1987=EDGE_LOOP('',(#5902,#5903,#5904,#5905));
#1988=EDGE_LOOP('',(#5906));
#1989=EDGE_LOOP('',(#5907));
#1990=EDGE_LOOP('',(#5908));
#1991=EDGE_LOOP('',(#5909));
#1992=EDGE_LOOP('',(#5910));
#1993=EDGE_LOOP('',(#5911));
#1994=EDGE_LOOP('',(#5912));
#1995=EDGE_LOOP('',(#5913));
#1996=EDGE_LOOP('',(#5914));
#1997=EDGE_LOOP('',(#5915));
#2534=LINE('',#12968,#2928);
#2535=LINE('',#12974,#2929);
#2536=LINE('',#12980,#2930);
#2537=LINE('',#12986,#2931);
#2538=LINE('',#12992,#2932);
#2539=LINE('',#12998,#2933);
#2540=LINE('',#13004,#2934);
#2541=LINE('',#13010,#2935);
#2542=LINE('',#13016,#2936);
#2543=LINE('',#13022,#2937);
#2544=LINE('',#13027,#2938);
#2545=LINE('',#13031,#2939);
#2546=LINE('',#13035,#2940);
#2547=LINE('',#13037,#2941);
#2548=LINE('',#13038,#2942);
#2549=LINE('',#13041,#2943);
#2550=LINE('',#13045,#2944);
#2551=LINE('',#13046,#2945);
#2928=VECTOR('',#10048,0.164999999999999);
#2929=VECTOR('',#10055,0.164999999999999);
#2930=VECTOR('',#10062,0.164999999999999);
#2931=VECTOR('',#10069,0.164999999999999);
#2932=VECTOR('',#10076,0.165);
#2933=VECTOR('',#10083,0.165);
#2934=VECTOR('',#10090,0.165);
#2935=VECTOR('',#10097,0.165);
#2936=VECTOR('',#10104,1.5);
#2937=VECTOR('',#10111,1.5);
#2938=VECTOR('',#10116,1.);
#2939=VECTOR('',#10119,1.);
#2940=VECTOR('',#10124,1.);
#2941=VECTOR('',#10125,1.);
#2942=VECTOR('',#10126,1.);
#2943=VECTOR('',#10129,1.);
#2944=VECTOR('',#10134,1.);
#2945=VECTOR('',#10135,1.);
#3294=CIRCLE('',#8365,0.164999999999999);
#3295=CIRCLE('',#8366,0.164999999999999);
#3296=CIRCLE('',#8368,0.164999999999999);
#3297=CIRCLE('',#8369,0.164999999999999);
#3298=CIRCLE('',#8371,0.164999999999999);
#3299=CIRCLE('',#8372,0.164999999999999);
#3300=CIRCLE('',#8374,0.164999999999999);
#3301=CIRCLE('',#8375,0.164999999999999);
#3302=CIRCLE('',#8377,0.165);
#3303=CIRCLE('',#8378,0.165);
#3304=CIRCLE('',#8380,0.165);
#3305=CIRCLE('',#8381,0.165);
#3306=CIRCLE('',#8383,0.165);
#3307=CIRCLE('',#8384,0.165);
#3308=CIRCLE('',#8386,0.165);
#3309=CIRCLE('',#8387,0.165);
#3310=CIRCLE('',#8389,1.5);
#3311=CIRCLE('',#8390,1.5);
#3312=CIRCLE('',#8392,1.5);
#3313=CIRCLE('',#8393,1.5);
#3314=CIRCLE('',#8395,2.2);
#3315=CIRCLE('',#8396,2.2);
#3316=CIRCLE('',#8399,2.2);
#3317=CIRCLE('',#8402,2.2);
#3824=VERTEX_POINT('',#12965);
#3825=VERTEX_POINT('',#12967);
#3826=VERTEX_POINT('',#12971);
#3827=VERTEX_POINT('',#12973);
#3828=VERTEX_POINT('',#12977);
#3829=VERTEX_POINT('',#12979);
#3830=VERTEX_POINT('',#12983);
#3831=VERTEX_POINT('',#12985);
#3832=VERTEX_POINT('',#12989);
#3833=VERTEX_POINT('',#12991);
#3834=VERTEX_POINT('',#12995);
#3835=VERTEX_POINT('',#12997);
#3836=VERTEX_POINT('',#13001);
#3837=VERTEX_POINT('',#13003);
#3838=VERTEX_POINT('',#13007);
#3839=VERTEX_POINT('',#13009);
#3840=VERTEX_POINT('',#13013);
#3841=VERTEX_POINT('',#13015);
#3842=VERTEX_POINT('',#13019);
#3843=VERTEX_POINT('',#13021);
#3844=VERTEX_POINT('',#13025);
#3845=VERTEX_POINT('',#13026);
#3846=VERTEX_POINT('',#13028);
#3847=VERTEX_POINT('',#13030);
#3848=VERTEX_POINT('',#13034);
#3849=VERTEX_POINT('',#13036);
#3850=VERTEX_POINT('',#13040);
#3851=VERTEX_POINT('',#13044);
#4547=EDGE_CURVE('',#3824,#3824,#3294,.T.);
#4548=EDGE_CURVE('',#3824,#3825,#2534,.T.);
#4549=EDGE_CURVE('',#3825,#3825,#3295,.T.);
#4550=EDGE_CURVE('',#3826,#3826,#3296,.T.);
#4551=EDGE_CURVE('',#3826,#3827,#2535,.T.);
#4552=EDGE_CURVE('',#3827,#3827,#3297,.T.);
#4553=EDGE_CURVE('',#3828,#3828,#3298,.T.);
#4554=EDGE_CURVE('',#3828,#3829,#2536,.T.);
#4555=EDGE_CURVE('',#3829,#3829,#3299,.T.);
#4556=EDGE_CURVE('',#3830,#3830,#3300,.T.);
#4557=EDGE_CURVE('',#3830,#3831,#2537,.T.);
#4558=EDGE_CURVE('',#3831,#3831,#3301,.T.);
#4559=EDGE_CURVE('',#3832,#3832,#3302,.T.);
#4560=EDGE_CURVE('',#3832,#3833,#2538,.T.);
#4561=EDGE_CURVE('',#3833,#3833,#3303,.T.);
#4562=EDGE_CURVE('',#3834,#3834,#3304,.T.);
#4563=EDGE_CURVE('',#3834,#3835,#2539,.T.);
#4564=EDGE_CURVE('',#3835,#3835,#3305,.T.);
#4565=EDGE_CURVE('',#3836,#3836,#3306,.T.);
#4566=EDGE_CURVE('',#3836,#3837,#2540,.T.);
#4567=EDGE_CURVE('',#3837,#3837,#3307,.T.);
#4568=EDGE_CURVE('',#3838,#3838,#3308,.T.);
#4569=EDGE_CURVE('',#3838,#3839,#2541,.T.);
#4570=EDGE_CURVE('',#3839,#3839,#3309,.T.);
#4571=EDGE_CURVE('',#3840,#3840,#3310,.T.);
#4572=EDGE_CURVE('',#3840,#3841,#2542,.T.);
#4573=EDGE_CURVE('',#3841,#3841,#3311,.T.);
#4574=EDGE_CURVE('',#3842,#3842,#3312,.T.);
#4575=EDGE_CURVE('',#3842,#3843,#2543,.T.);
#4576=EDGE_CURVE('',#3843,#3843,#3313,.T.);
#4577=EDGE_CURVE('',#3844,#3845,#2544,.T.);
#4578=EDGE_CURVE('',#3846,#3844,#3314,.T.);
#4579=EDGE_CURVE('',#3847,#3846,#2545,.T.);
#4580=EDGE_CURVE('',#3847,#3845,#3315,.T.);
#4581=EDGE_CURVE('',#3848,#3845,#2546,.T.);
#4582=EDGE_CURVE('',#3849,#3848,#2547,.T.);
#4583=EDGE_CURVE('',#3844,#3849,#2548,.T.);
#4584=EDGE_CURVE('',#3847,#3850,#2549,.T.);
#4585=EDGE_CURVE('',#3848,#3850,#3316,.T.);
#4586=EDGE_CURVE('',#3851,#3846,#2550,.T.);
#4587=EDGE_CURVE('',#3850,#3851,#2551,.T.);
#4588=EDGE_CURVE('',#3849,#3851,#3317,.T.);
#5832=ORIENTED_EDGE('',*,*,#4547,.F.);
#5833=ORIENTED_EDGE('',*,*,#4548,.T.);
#5834=ORIENTED_EDGE('',*,*,#4549,.F.);
#5835=ORIENTED_EDGE('',*,*,#4548,.F.);
#5836=ORIENTED_EDGE('',*,*,#4550,.F.);
#5837=ORIENTED_EDGE('',*,*,#4551,.T.);
#5838=ORIENTED_EDGE('',*,*,#4552,.F.);
#5839=ORIENTED_EDGE('',*,*,#4551,.F.);
#5840=ORIENTED_EDGE('',*,*,#4553,.F.);
#5841=ORIENTED_EDGE('',*,*,#4554,.T.);
#5842=ORIENTED_EDGE('',*,*,#4555,.F.);
#5843=ORIENTED_EDGE('',*,*,#4554,.F.);
#5844=ORIENTED_EDGE('',*,*,#4556,.F.);
#5845=ORIENTED_EDGE('',*,*,#4557,.T.);
#5846=ORIENTED_EDGE('',*,*,#4558,.F.);
#5847=ORIENTED_EDGE('',*,*,#4557,.F.);
#5848=ORIENTED_EDGE('',*,*,#4559,.F.);
#5849=ORIENTED_EDGE('',*,*,#4560,.T.);
#5850=ORIENTED_EDGE('',*,*,#4561,.F.);
#5851=ORIENTED_EDGE('',*,*,#4560,.F.);
#5852=ORIENTED_EDGE('',*,*,#4562,.F.);
#5853=ORIENTED_EDGE('',*,*,#4563,.T.);
#5854=ORIENTED_EDGE('',*,*,#4564,.F.);
#5855=ORIENTED_EDGE('',*,*,#4563,.F.);
#5856=ORIENTED_EDGE('',*,*,#4565,.F.);
#5857=ORIENTED_EDGE('',*,*,#4566,.T.);
#5858=ORIENTED_EDGE('',*,*,#4567,.F.);
#5859=ORIENTED_EDGE('',*,*,#4566,.F.);
#5860=ORIENTED_EDGE('',*,*,#4568,.F.);
#5861=ORIENTED_EDGE('',*,*,#4569,.T.);
#5862=ORIENTED_EDGE('',*,*,#4570,.F.);
#5863=ORIENTED_EDGE('',*,*,#4569,.F.);
#5864=ORIENTED_EDGE('',*,*,#4571,.F.);
#5865=ORIENTED_EDGE('',*,*,#4572,.T.);
#5866=ORIENTED_EDGE('',*,*,#4573,.F.);
#5867=ORIENTED_EDGE('',*,*,#4572,.F.);
#5868=ORIENTED_EDGE('',*,*,#4574,.F.);
#5869=ORIENTED_EDGE('',*,*,#4575,.T.);
#5870=ORIENTED_EDGE('',*,*,#4576,.F.);
#5871=ORIENTED_EDGE('',*,*,#4575,.F.);
#5872=ORIENTED_EDGE('',*,*,#4577,.F.);
#5873=ORIENTED_EDGE('',*,*,#4578,.F.);
#5874=ORIENTED_EDGE('',*,*,#4579,.F.);
#5875=ORIENTED_EDGE('',*,*,#4580,.T.);
#5876=ORIENTED_EDGE('',*,*,#4577,.T.);
#5877=ORIENTED_EDGE('',*,*,#4581,.F.);
#5878=ORIENTED_EDGE('',*,*,#4582,.F.);
#5879=ORIENTED_EDGE('',*,*,#4583,.F.);
#5880=ORIENTED_EDGE('',*,*,#4580,.F.);
#5881=ORIENTED_EDGE('',*,*,#4584,.T.);
#5882=ORIENTED_EDGE('',*,*,#4585,.F.);
#5883=ORIENTED_EDGE('',*,*,#4581,.T.);
#5884=ORIENTED_EDGE('',*,*,#4559,.T.);
#5885=ORIENTED_EDGE('',*,*,#4562,.T.);
#5886=ORIENTED_EDGE('',*,*,#4565,.T.);
#5887=ORIENTED_EDGE('',*,*,#4568,.T.);
#5888=ORIENTED_EDGE('',*,*,#4571,.T.);
#5889=ORIENTED_EDGE('',*,*,#4574,.T.);
#5890=ORIENTED_EDGE('',*,*,#4556,.T.);
#5891=ORIENTED_EDGE('',*,*,#4553,.T.);
#5892=ORIENTED_EDGE('',*,*,#4550,.T.);
#5893=ORIENTED_EDGE('',*,*,#4547,.T.);
#5894=ORIENTED_EDGE('',*,*,#4579,.T.);
#5895=ORIENTED_EDGE('',*,*,#4586,.F.);
#5896=ORIENTED_EDGE('',*,*,#4587,.F.);
#5897=ORIENTED_EDGE('',*,*,#4584,.F.);
#5898=ORIENTED_EDGE('',*,*,#4582,.T.);
#5899=ORIENTED_EDGE('',*,*,#4585,.T.);
#5900=ORIENTED_EDGE('',*,*,#4587,.T.);
#5901=ORIENTED_EDGE('',*,*,#4588,.F.);
#5902=ORIENTED_EDGE('',*,*,#4583,.T.);
#5903=ORIENTED_EDGE('',*,*,#4588,.T.);
#5904=ORIENTED_EDGE('',*,*,#4586,.T.);
#5905=ORIENTED_EDGE('',*,*,#4578,.T.);
#5906=ORIENTED_EDGE('',*,*,#4561,.T.);
#5907=ORIENTED_EDGE('',*,*,#4564,.T.);
#5908=ORIENTED_EDGE('',*,*,#4567,.T.);
#5909=ORIENTED_EDGE('',*,*,#4570,.T.);
#5910=ORIENTED_EDGE('',*,*,#4573,.T.);
#5911=ORIENTED_EDGE('',*,*,#4576,.T.);
#5912=ORIENTED_EDGE('',*,*,#4558,.T.);
#5913=ORIENTED_EDGE('',*,*,#4555,.T.);
#5914=ORIENTED_EDGE('',*,*,#4552,.T.);
#5915=ORIENTED_EDGE('',*,*,#4549,.T.);
#6808=CYLINDRICAL_SURFACE('',#8364,0.164999999999999);
#6809=CYLINDRICAL_SURFACE('',#8367,0.164999999999999);
#6810=CYLINDRICAL_SURFACE('',#8370,0.164999999999999);
#6811=CYLINDRICAL_SURFACE('',#8373,0.164999999999999);
#6812=CYLINDRICAL_SURFACE('',#8376,0.165);
#6813=CYLINDRICAL_SURFACE('',#8379,0.165);
#6814=CYLINDRICAL_SURFACE('',#8382,0.165);
#6815=CYLINDRICAL_SURFACE('',#8385,0.165);
#6816=CYLINDRICAL_SURFACE('',#8388,1.5);
#6817=CYLINDRICAL_SURFACE('',#8391,1.5);
#6818=CYLINDRICAL_SURFACE('',#8394,2.2);
#6819=CYLINDRICAL_SURFACE('',#8401,2.2);
#7109=ADVANCED_FACE('',(#1404),#6808,.F.);
#7110=ADVANCED_FACE('',(#1405),#6809,.F.);
#7111=ADVANCED_FACE('',(#1406),#6810,.F.);
#7112=ADVANCED_FACE('',(#1407),#6811,.F.);
#7113=ADVANCED_FACE('',(#1408),#6812,.F.);
#7114=ADVANCED_FACE('',(#1409),#6813,.F.);
#7115=ADVANCED_FACE('',(#1410),#6814,.F.);
#7116=ADVANCED_FACE('',(#1411),#6815,.F.);
#7117=ADVANCED_FACE('',(#1412),#6816,.F.);
#7118=ADVANCED_FACE('',(#1413),#6817,.F.);
#7119=ADVANCED_FACE('',(#1414),#6818,.T.);
#7120=ADVANCED_FACE('',(#1415),#1111,.T.);
#7121=ADVANCED_FACE('',(#1416,#873,#874,#875,#876,#877,#878,#879,#880,#881,
#882),#1112,.F.);
#7122=ADVANCED_FACE('',(#1417),#1113,.T.);
#7123=ADVANCED_FACE('',(#1418),#6819,.T.);
#7124=ADVANCED_FACE('',(#1419,#883,#884,#885,#886,#887,#888,#889,#890,#891,
#892),#1114,.T.);
#7352=CLOSED_SHELL('',(#7109,#7110,#7111,#7112,#7113,#7114,#7115,#7116,
#7117,#7118,#7119,#7120,#7121,#7122,#7123,#7124));
#8363=AXIS2_PLACEMENT_3D('',#12963,#10042,#10043);
#8364=AXIS2_PLACEMENT_3D('',#12964,#10044,#10045);
#8365=AXIS2_PLACEMENT_3D('',#12966,#10046,#10047);
#8366=AXIS2_PLACEMENT_3D('',#12969,#10049,#10050);
#8367=AXIS2_PLACEMENT_3D('',#12970,#10051,#10052);
#8368=AXIS2_PLACEMENT_3D('',#12972,#10053,#10054);
#8369=AXIS2_PLACEMENT_3D('',#12975,#10056,#10057);
#8370=AXIS2_PLACEMENT_3D('',#12976,#10058,#10059);
#8371=AXIS2_PLACEMENT_3D('',#12978,#10060,#10061);
#8372=AXIS2_PLACEMENT_3D('',#12981,#10063,#10064);
#8373=AXIS2_PLACEMENT_3D('',#12982,#10065,#10066);
#8374=AXIS2_PLACEMENT_3D('',#12984,#10067,#10068);
#8375=AXIS2_PLACEMENT_3D('',#12987,#10070,#10071);
#8376=AXIS2_PLACEMENT_3D('',#12988,#10072,#10073);
#8377=AXIS2_PLACEMENT_3D('',#12990,#10074,#10075);
#8378=AXIS2_PLACEMENT_3D('',#12993,#10077,#10078);
#8379=AXIS2_PLACEMENT_3D('',#12994,#10079,#10080);
#8380=AXIS2_PLACEMENT_3D('',#12996,#10081,#10082);
#8381=AXIS2_PLACEMENT_3D('',#12999,#10084,#10085);
#8382=AXIS2_PLACEMENT_3D('',#13000,#10086,#10087);
#8383=AXIS2_PLACEMENT_3D('',#13002,#10088,#10089);
#8384=AXIS2_PLACEMENT_3D('',#13005,#10091,#10092);
#8385=AXIS2_PLACEMENT_3D('',#13006,#10093,#10094);
#8386=AXIS2_PLACEMENT_3D('',#13008,#10095,#10096);
#8387=AXIS2_PLACEMENT_3D('',#13011,#10098,#10099);
#8388=AXIS2_PLACEMENT_3D('',#13012,#10100,#10101);
#8389=AXIS2_PLACEMENT_3D('',#13014,#10102,#10103);
#8390=AXIS2_PLACEMENT_3D('',#13017,#10105,#10106);
#8391=AXIS2_PLACEMENT_3D('',#13018,#10107,#10108);
#8392=AXIS2_PLACEMENT_3D('',#13020,#10109,#10110);
#8393=AXIS2_PLACEMENT_3D('',#13023,#10112,#10113);
#8394=AXIS2_PLACEMENT_3D('',#13024,#10114,#10115);
#8395=AXIS2_PLACEMENT_3D('',#13029,#10117,#10118);
#8396=AXIS2_PLACEMENT_3D('',#13032,#10120,#10121);
#8397=AXIS2_PLACEMENT_3D('',#13033,#10122,#10123);
#8398=AXIS2_PLACEMENT_3D('',#13039,#10127,#10128);
#8399=AXIS2_PLACEMENT_3D('',#13042,#10130,#10131);
#8400=AXIS2_PLACEMENT_3D('',#13043,#10132,#10133);
#8401=AXIS2_PLACEMENT_3D('',#13047,#10136,#10137);
#8402=AXIS2_PLACEMENT_3D('',#13048,#10138,#10139);
#8403=AXIS2_PLACEMENT_3D('',#13049,#10140,#10141);
#10042=DIRECTION('axis',(0.,0.,1.));
#10043=DIRECTION('refdir',(1.,0.,0.));
#10044=DIRECTION('center_axis',(0.,1.,0.));
#10045=DIRECTION('ref_axis',(1.,0.,0.));
#10046=DIRECTION('center_axis',(0.,1.,0.));
#10047=DIRECTION('ref_axis',(1.,0.,0.));
#10048=DIRECTION('',(0.,1.,0.));
#10049=DIRECTION('center_axis',(0.,-1.,0.));
#10050=DIRECTION('ref_axis',(1.,0.,0.));
#10051=DIRECTION('center_axis',(0.,1.,0.));
#10052=DIRECTION('ref_axis',(1.,0.,0.));
#10053=DIRECTION('center_axis',(0.,1.,0.));
#10054=DIRECTION('ref_axis',(1.,0.,0.));
#10055=DIRECTION('',(0.,1.,0.));
#10056=DIRECTION('center_axis',(0.,-1.,0.));
#10057=DIRECTION('ref_axis',(1.,0.,0.));
#10058=DIRECTION('center_axis',(0.,1.,0.));
#10059=DIRECTION('ref_axis',(1.,0.,0.));
#10060=DIRECTION('center_axis',(0.,1.,0.));
#10061=DIRECTION('ref_axis',(1.,0.,0.));
#10062=DIRECTION('',(0.,1.,0.));
#10063=DIRECTION('center_axis',(0.,-1.,0.));
#10064=DIRECTION('ref_axis',(1.,0.,0.));
#10065=DIRECTION('center_axis',(0.,1.,0.));
#10066=DIRECTION('ref_axis',(1.,0.,0.));
#10067=DIRECTION('center_axis',(0.,1.,0.));
#10068=DIRECTION('ref_axis',(1.,0.,0.));
#10069=DIRECTION('',(0.,1.,0.));
#10070=DIRECTION('center_axis',(0.,-1.,0.));
#10071=DIRECTION('ref_axis',(1.,0.,0.));
#10072=DIRECTION('center_axis',(0.,1.,0.));
#10073=DIRECTION('ref_axis',(1.,0.,0.));
#10074=DIRECTION('center_axis',(0.,1.,0.));
#10075=DIRECTION('ref_axis',(1.,0.,0.));
#10076=DIRECTION('',(0.,1.,0.));
#10077=DIRECTION('center_axis',(0.,-1.,0.));
#10078=DIRECTION('ref_axis',(1.,0.,0.));
#10079=DIRECTION('center_axis',(0.,1.,0.));
#10080=DIRECTION('ref_axis',(1.,0.,0.));
#10081=DIRECTION('center_axis',(0.,1.,0.));
#10082=DIRECTION('ref_axis',(1.,0.,0.));
#10083=DIRECTION('',(0.,1.,0.));
#10084=DIRECTION('center_axis',(0.,-1.,0.));
#10085=DIRECTION('ref_axis',(1.,0.,0.));
#10086=DIRECTION('center_axis',(0.,1.,0.));
#10087=DIRECTION('ref_axis',(1.,0.,0.));
#10088=DIRECTION('center_axis',(0.,1.,0.));
#10089=DIRECTION('ref_axis',(1.,0.,0.));
#10090=DIRECTION('',(0.,1.,0.));
#10091=DIRECTION('center_axis',(0.,-1.,0.));
#10092=DIRECTION('ref_axis',(1.,0.,0.));
#10093=DIRECTION('center_axis',(0.,1.,0.));
#10094=DIRECTION('ref_axis',(1.,0.,0.));
#10095=DIRECTION('center_axis',(0.,1.,0.));
#10096=DIRECTION('ref_axis',(1.,0.,0.));
#10097=DIRECTION('',(0.,1.,0.));
#10098=DIRECTION('center_axis',(0.,-1.,0.));
#10099=DIRECTION('ref_axis',(1.,0.,0.));
#10100=DIRECTION('center_axis',(0.,1.,0.));
#10101=DIRECTION('ref_axis',(1.,0.,0.));
#10102=DIRECTION('center_axis',(0.,1.,0.));
#10103=DIRECTION('ref_axis',(1.,0.,0.));
#10104=DIRECTION('',(0.,1.,0.));
#10105=DIRECTION('center_axis',(0.,-1.,0.));
#10106=DIRECTION('ref_axis',(1.,0.,0.));
#10107=DIRECTION('center_axis',(0.,1.,0.));
#10108=DIRECTION('ref_axis',(1.,0.,0.));
#10109=DIRECTION('center_axis',(0.,1.,0.));
#10110=DIRECTION('ref_axis',(1.,0.,0.));
#10111=DIRECTION('',(0.,1.,0.));
#10112=DIRECTION('center_axis',(0.,-1.,0.));
#10113=DIRECTION('ref_axis',(1.,0.,0.));
#10114=DIRECTION('center_axis',(0.,1.,0.));
#10115=DIRECTION('ref_axis',(1.,0.,0.));
#10116=DIRECTION('',(0.,-1.,0.));
#10117=DIRECTION('center_axis',(0.,1.,0.));
#10118=DIRECTION('ref_axis',(1.,0.,0.));
#10119=DIRECTION('',(0.,1.,0.));
#10120=DIRECTION('center_axis',(0.,1.,0.));
#10121=DIRECTION('ref_axis',(1.,0.,0.));
#10122=DIRECTION('center_axis',(0.,0.,-1.));
#10123=DIRECTION('ref_axis',(-1.,0.,0.));
#10124=DIRECTION('',(1.,0.,0.));
#10125=DIRECTION('',(0.,-1.,0.));
#10126=DIRECTION('',(-1.,0.,0.));
#10127=DIRECTION('center_axis',(0.,1.,0.));
#10128=DIRECTION('ref_axis',(1.,0.,0.));
#10129=DIRECTION('',(-1.,0.,0.));
#10130=DIRECTION('center_axis',(0.,1.,0.));
#10131=DIRECTION('ref_axis',(1.,0.,0.));
#10132=DIRECTION('center_axis',(0.,0.,1.));
#10133=DIRECTION('ref_axis',(1.,0.,0.));
#10134=DIRECTION('',(1.,0.,0.));
#10135=DIRECTION('',(0.,1.,0.));
#10136=DIRECTION('center_axis',(0.,1.,0.));
#10137=DIRECTION('ref_axis',(-1.,0.,-1.22464679914735E-16));
#10138=DIRECTION('center_axis',(0.,1.,0.));
#10139=DIRECTION('ref_axis',(1.,0.,0.));
#10140=DIRECTION('center_axis',(0.,1.,0.));
#10141=DIRECTION('ref_axis',(1.,0.,0.));
#12963=CARTESIAN_POINT('',(0.,0.,0.));
#12964=CARTESIAN_POINT('Origin',(18.7625631329235,-1.15,12.7625631329235));
#12965=CARTESIAN_POINT('',(18.5975631329235,-1.05,12.7625631329235));
#12966=CARTESIAN_POINT('Origin',(18.7625631329235,-1.05,12.7625631329235));
#12967=CARTESIAN_POINT('',(18.5975631329235,1.05,12.7625631329235));
#12968=CARTESIAN_POINT('',(18.5975631329235,-1.15,12.7625631329235));
#12969=CARTESIAN_POINT('Origin',(18.7625631329235,1.05,12.7625631329235));
#12970=CARTESIAN_POINT('Origin',(18.7625631329235,-1.15,15.2374368670765));
#12971=CARTESIAN_POINT('',(18.5975631329235,-1.05,15.2374368670765));
#12972=CARTESIAN_POINT('Origin',(18.7625631329235,-1.05,15.2374368670765));
#12973=CARTESIAN_POINT('',(18.5975631329235,1.05,15.2374368670765));
#12974=CARTESIAN_POINT('',(18.5975631329235,-1.15,15.2374368670765));
#12975=CARTESIAN_POINT('Origin',(18.7625631329235,1.05,15.2374368670765));
#12976=CARTESIAN_POINT('Origin',(21.2374368670765,-1.15,15.2374368670765));
#12977=CARTESIAN_POINT('',(21.0724368670765,-1.05,15.2374368670765));
#12978=CARTESIAN_POINT('Origin',(21.2374368670765,-1.05,15.2374368670765));
#12979=CARTESIAN_POINT('',(21.0724368670765,1.05,15.2374368670765));
#12980=CARTESIAN_POINT('',(21.0724368670765,-1.15,15.2374368670765));
#12981=CARTESIAN_POINT('Origin',(21.2374368670765,1.05,15.2374368670765));
#12982=CARTESIAN_POINT('Origin',(21.2374368670765,-1.15,12.7625631329235));
#12983=CARTESIAN_POINT('',(21.0724368670765,-1.05,12.7625631329235));
#12984=CARTESIAN_POINT('Origin',(21.2374368670765,-1.05,12.7625631329235));
#12985=CARTESIAN_POINT('',(21.0724368670765,1.05,12.7625631329235));
#12986=CARTESIAN_POINT('',(21.0724368670765,-1.15,12.7625631329235));
#12987=CARTESIAN_POINT('Origin',(21.2374368670765,1.05,12.7625631329235));
#12988=CARTESIAN_POINT('Origin',(-1.23743686707646,-1.15,12.7625631329235));
#12989=CARTESIAN_POINT('',(-1.40243686707646,-1.05,12.7625631329235));
#12990=CARTESIAN_POINT('Origin',(-1.23743686707646,-1.05,12.7625631329235));
#12991=CARTESIAN_POINT('',(-1.40243686707646,1.05,12.7625631329235));
#12992=CARTESIAN_POINT('',(-1.40243686707646,-1.15,12.7625631329235));
#12993=CARTESIAN_POINT('Origin',(-1.23743686707646,1.05,12.7625631329235));
#12994=CARTESIAN_POINT('Origin',(-1.23743686707646,-1.15,15.2374368670765));
#12995=CARTESIAN_POINT('',(-1.40243686707646,-1.05,15.2374368670765));
#12996=CARTESIAN_POINT('Origin',(-1.23743686707646,-1.05,15.2374368670765));
#12997=CARTESIAN_POINT('',(-1.40243686707646,1.05,15.2374368670765));
#12998=CARTESIAN_POINT('',(-1.40243686707646,-1.15,15.2374368670765));
#12999=CARTESIAN_POINT('Origin',(-1.23743686707646,1.05,15.2374368670765));
#13000=CARTESIAN_POINT('Origin',(1.23743686707646,-1.15,15.2374368670765));
#13001=CARTESIAN_POINT('',(1.07243686707646,-1.05,15.2374368670765));
#13002=CARTESIAN_POINT('Origin',(1.23743686707646,-1.05,15.2374368670765));
#13003=CARTESIAN_POINT('',(1.07243686707646,1.05,15.2374368670765));
#13004=CARTESIAN_POINT('',(1.07243686707646,-1.15,15.2374368670765));
#13005=CARTESIAN_POINT('Origin',(1.23743686707646,1.05,15.2374368670765));
#13006=CARTESIAN_POINT('Origin',(1.23743686707646,-1.15,12.7625631329235));
#13007=CARTESIAN_POINT('',(1.07243686707646,-1.05,12.7625631329235));
#13008=CARTESIAN_POINT('Origin',(1.23743686707646,-1.05,12.7625631329235));
#13009=CARTESIAN_POINT('',(1.07243686707646,1.05,12.7625631329235));
#13010=CARTESIAN_POINT('',(1.07243686707646,-1.15,12.7625631329235));
#13011=CARTESIAN_POINT('Origin',(1.23743686707646,1.05,12.7625631329235));
#13012=CARTESIAN_POINT('Origin',(0.,-1.15,14.));
#13013=CARTESIAN_POINT('',(-1.5,-1.05,14.));
#13014=CARTESIAN_POINT('Origin',(0.,-1.05,14.));
#13015=CARTESIAN_POINT('',(-1.5,1.05,14.));
#13016=CARTESIAN_POINT('',(-1.5,-1.15,14.));
#13017=CARTESIAN_POINT('Origin',(0.,1.05,14.));
#13018=CARTESIAN_POINT('Origin',(20.,-1.15,14.));
#13019=CARTESIAN_POINT('',(18.5,-1.05,14.));
#13020=CARTESIAN_POINT('Origin',(20.,-1.05,14.));
#13021=CARTESIAN_POINT('',(18.5,1.05,14.));
#13022=CARTESIAN_POINT('',(18.5,-1.15,14.));
#13023=CARTESIAN_POINT('Origin',(20.,1.05,14.));
#13024=CARTESIAN_POINT('Origin',(20.,-1.05,14.));
#13025=CARTESIAN_POINT('',(17.9506098468081,1.05,13.2));
#13026=CARTESIAN_POINT('',(17.9506098468081,-1.05,13.2));
#13027=CARTESIAN_POINT('',(17.9506098468081,-1.05,13.2));
#13028=CARTESIAN_POINT('',(17.9506098468081,1.05,14.8));
#13029=CARTESIAN_POINT('Origin',(20.,1.05,14.));
#13030=CARTESIAN_POINT('',(17.9506098468081,-1.05,14.8));
#13031=CARTESIAN_POINT('',(17.9506098468081,-1.05,14.8));
#13032=CARTESIAN_POINT('Origin',(20.,-1.05,14.));
#13033=CARTESIAN_POINT('Origin',(20.,-1.05,13.2));
#13034=CARTESIAN_POINT('',(2.04939015319192,-1.05,13.2));
#13035=CARTESIAN_POINT('',(0.,-1.05,13.2));
#13036=CARTESIAN_POINT('',(2.04939015319192,1.05,13.2));
#13037=CARTESIAN_POINT('',(2.04939015319192,-1.05,13.2));
#13038=CARTESIAN_POINT('',(0.,1.05,13.2));
#13039=CARTESIAN_POINT('Origin',(0.,-1.05,14.));
#13040=CARTESIAN_POINT('',(2.04939015319192,-1.05,14.8));
#13041=CARTESIAN_POINT('',(20.,-1.05,14.8));
#13042=CARTESIAN_POINT('Origin',(0.,-1.05,14.));
#13043=CARTESIAN_POINT('Origin',(0.,-1.05,14.8));
#13044=CARTESIAN_POINT('',(2.04939015319192,1.05,14.8));
#13045=CARTESIAN_POINT('',(20.,1.05,14.8));
#13046=CARTESIAN_POINT('',(2.04939015319192,-1.05,14.8));
#13047=CARTESIAN_POINT('Origin',(0.,-1.05,14.));
#13048=CARTESIAN_POINT('Origin',(0.,1.05,14.));
#13049=CARTESIAN_POINT('Origin',(0.,1.05,14.));
#14428=UNCERTAINTY_MEASURE_WITH_UNIT(LENGTH_MEASURE(0.001),#14513,
'DISTANCE_ACCURACY_VALUE',
'Maximum model space distance between geometric entities at asserted c
onnectivities');
#14455=UNCERTAINTY_MEASURE_WITH_UNIT(LENGTH_MEASURE(0.001),#14513,
'DISTANCE_ACCURACY_VALUE',
'Maximum model space distance between geometric entities at asserted c
onnectivities');
#14485=(
GEOMETRIC_REPRESENTATION_CONTEXT(3)
GLOBAL_UNCERTAINTY_ASSIGNED_CONTEXT((#14428))
GLOBAL_UNIT_ASSIGNED_CONTEXT((#14513,#14515,#14516))
REPRESENTATION_CONTEXT('','3D')
);
#14512=(
GEOMETRIC_REPRESENTATION_CONTEXT(3)
GLOBAL_UNCERTAINTY_ASSIGNED_CONTEXT((#14455))
GLOBAL_UNIT_ASSIGNED_CONTEXT((#14513,#14515,#14516))
REPRESENTATION_CONTEXT('','3D')
);
#14513=(
LENGTH_UNIT()
NAMED_UNIT(*)
SI_UNIT(.CENTI.,.METRE.)
);
#14515=(
NAMED_UNIT(*)
PLANE_ANGLE_UNIT()
SI_UNIT($,.RADIAN.)
);
#14516=(
NAMED_UNIT(*)
SI_UNIT($,.STERADIAN.)
SOLID_ANGLE_UNIT()
);
#14546=SHAPE_DEFINITION_REPRESENTATION(#14602,#14770);
#14602=PRODUCT_DEFINITION_SHAPE('',$,#14827);
#14770=SHAPE_REPRESENTATION('',(#8363),#14485);
#14797=PRODUCT_DEFINITION_CONTEXT('part definition',#14967,'design');
#14827=PRODUCT_DEFINITION('200 mm arm (1)','200 mm arm (1)',#14883,#14797);
#14883=PRODUCT_DEFINITION_FORMATION('',$,#14998);
#14967=APPLICATION_CONTEXT(
'Core Data for Automotive Mechanical Design Process');
#14968=PRODUCT_CONTEXT('part definition',#14967,'mechanical');
#14998=PRODUCT('200 mm arm (1)','200 mm arm (1)','200 mm arm (1)',(#14968));
#15095=COLOUR_RGB('Off White',0.89,0.88,0.83);
#15096=FILL_AREA_STYLE_COLOUR('',#15095);
#15097=FILL_AREA_STYLE('',(#15096));
#15098=SURFACE_STYLE_FILL_AREA(#15097);
#15099=SURFACE_SIDE_STYLE('',(#15098));
#15100=SURFACE_STYLE_USAGE(.BOTH.,#15099);
#15101=PRESENTATION_STYLE_ASSIGNMENT((#15100));
ENDSEC;
END-ISO-10303-21;
